ISO-10303-21;
HEADER;
/* Generated by software containing ST-Developer
 * from STEP Tools, Inc. (www.steptools.com) 
 */

FILE_DESCRIPTION(
/* description */ ('Drill jig with bushing plate'),
/* implementation_level */ '2;1');

FILE_NAME(
/* name */ 'Bonded foot (1).step',
/* time_stamp */ '2026-10-27T10:51:08-07:00',
/* author */ (''),
/* organization */ (''),
/* preprocessor_version */ 'ST-DEVELOPER v20.2',
/* originating_system */ 'Autodesk Translation Framework v15.17.0.0',
/* authorisation */ '');

FILE_SCHEMA (('AUTOMOTIVE_DESIGN { 1 0 10303 214 3 1 1 }'));
ENDSEC;

DATA;
#10=MECHANICAL_DESIGN_GEOMETRIC_PRESENTATION_REPRESENTATION('',(#225),#6638);
#177=SHAPE_REPRESENTATION_RELATIONSHIP('SRR','None',#6741,#201);
#201=ADVANCED_BREP_SHAPE_REPRESENTATION('',(#249),#6614);
#225=STYLED_ITEM('',(#6957),#249);
#249=MANIFOLD_SOLID_BREP('Body1',#3592);
#378=PLANE('',#3942);
#379=PLANE('',#3943);
#524=FACE_OUTER_BOUND('',#766,.T.);
#525=FACE_OUTER_BOUND('',#767,.T.);
#526=FACE_OUTER_BOUND('',#768,.T.);
#766=EDGE_LOOP('',(#2551,#2552,#2553,#2554));
#767=EDGE_LOOP('',(#2555));
#768=EDGE_LOOP('',(#2556));
#1057=LINE('',#5613,#1318);
#1318=VECTOR('',#4476,0.800000000000001);
#1582=CIRCLE('',#3940,0.800000000000001);
#1583=CIRCLE('',#3941,0.800000000000001);
#1758=VERTEX_POINT('',#5610);
#1759=VERTEX_POINT('',#5612);
#2063=EDGE_CURVE('',#1758,#1758,#1582,.T.);
#2064=EDGE_CURVE('',#1758,#1759,#1057,.T.);
#2065=EDGE_CURVE('',#1759,#1759,#1583,.T.);
#2551=ORIENTED_EDGE('',*,*,#2063,.F.);
#2552=ORIENTED_EDGE('',*,*,#2064,.T.);
#2553=ORIENTED_EDGE('',*,*,#2065,.T.);
#2554=ORIENTED_EDGE('',*,*,#2064,.F.);
#2555=ORIENTED_EDGE('',*,*,#2063,.T.);
#2556=ORIENTED_EDGE('',*,*,#2065,.F.);
#3314=CYLINDRICAL_SURFACE('',#3939,0.800000000000001);
#3399=ADVANCED_FACE('',(#524),#3314,.T.);
#3400=ADVANCED_FACE('',(#525),#378,.T.);
#3401=ADVANCED_FACE('',(#526),#379,.F.);
#3592=CLOSED_SHELL('',(#3399,#3400,#3401));
#3938=AXIS2_PLACEMENT_3D('',#5608,#4470,#4471);
#3939=AXIS2_PLACEMENT_3D('',#5609,#4472,#4473);
#3940=AXIS2_PLACEMENT_3D('',#5611,#4474,#4475);
#3941=AXIS2_PLACEMENT_3D('',#5614,#4477,#4478);
#3942=AXIS2_PLACEMENT_3D('',#5615,#4479,#4480);
#3943=AXIS2_PLACEMENT_3D('',#5616,#4481,#4482);
#4470=DIRECTION('axis',(0.,0.,1.));
#4471=DIRECTION('refdir',(1.,0.,0.));
#4472=DIRECTION('center_axis',(0.,0.,1.));
#4473=DIRECTION('ref_axis',(1.,0.,0.));
#4474=DIRECTION('center_axis',(0.,0.,1.));
#4475=DIRECTION('ref_axis',(1.,0.,0.));
#4476=DIRECTION('',(0.,0.,-1.));
#4477=DIRECTION('center_axis',(0.,0.,1.));
#4478=DIRECTION('ref_axis',(1.,0.,0.));
#4479=DIRECTION('center_axis',(0.,0.,1.));
#4480=DIRECTION('ref_axis',(1.,0.,0.));
#4481=DIRECTION('center_axis',(0.,0.,1.));
#4482=DIRECTION('ref_axis',(1.,0.,0.));
#5608=CARTESIAN_POINT('',(0.,0.,0.));
#5609=CARTESIAN_POINT('Origin',(-9.,7.,-0.5));
#5610=CARTESIAN_POINT('',(-9.8,7.,0.));
#5611=CARTESIAN_POINT('Origin',(-9.,7.,0.));
#5612=CARTESIAN_POINT('',(-9.8,7.,-0.5));
#5613=CARTESIAN_POINT('',(-9.8,7.,-0.5));
#5614=CARTESIAN_POINT('Origin',(-9.,7.,-0.5));
#5615=CARTESIAN_POINT('Origin',(-9.,7.,0.));
#5616=CARTESIAN_POINT('Origin',(-9.,7.,-0.5));
#6585=UNCERTAINTY_MEASURE_WITH_UNIT(LENGTH_MEASURE(0.001),#6639,
'DISTANCE_ACCURACY_VALUE',
'Maximum model space distance between geometric entities at asserted c
onnectivities');
#6609=UNCERTAINTY_MEASURE_WITH_UNIT(LENGTH_MEASURE(0.001),#6639,
'DISTANCE_ACCURACY_VALUE',
'Maximum model space distance between geometric entities at asserted c
onnectivities');
#6614=(
GEOMETRIC_REPRESENTATION_CONTEXT(3)
GLOBAL_UNCERTAINTY_ASSIGNED_CONTEXT((#6585))
GLOBAL_UNIT_ASSIGNED_CONTEXT((#6639,#6641,#6642))
REPRESENTATION_CONTEXT('','3D')
);
#6638=(
GEOMETRIC_REPRESENTATION_CONTEXT(3)
GLOBAL_UNCERTAINTY_ASSIGNED_CONTEXT((#6609))
GLOBAL_UNIT_ASSIGNED_CONTEXT((#6639,#6641,#6642))
REPRESENTATION_CONTEXT('','3D')
);
#6639=(
LENGTH_UNIT()
NAMED_UNIT(*)
SI_UNIT(.CENTI.,.METRE.)
);
#6641=(
NAMED_UNIT(*)
PLANE_ANGLE_UNIT()
SI_UNIT($,.RADIAN.)
);
#6642=(
NAMED_UNIT(*)
SI_UNIT($,.STERADIAN.)
SOLID_ANGLE_UNIT()
);
#6647=SHAPE_DEFINITION_REPRESENTATION(#6675,#6741);
#6675=PRODUCT_DEFINITION_SHAPE('',$,#6770);
#6741=SHAPE_REPRESENTATION('',(#3938),#6614);
#6765=PRODUCT_DEFINITION_CONTEXT('part definition',#6851,'design');
#6770=PRODUCT_DEFINITION('Bonded foot (1)','Bonded foot (1)',#6798,#6765);
#6798=PRODUCT_DEFINITION_FORMATION('',$,#6857);
#6851=APPLICATION_CONTEXT(
'Core Data for Automotive Mechanical Design Process');
#6852=PRODUCT_CONTEXT('part definition',#6851,'mechanical');
#6857=PRODUCT('Bonded foot (1)','Bonded foot (1)','Bonded foot (1)',(#6852));
#6951=COLOUR_RGB('Off White',0.89,0.88,0.83);
#6952=FILL_AREA_STYLE_COLOUR('',#6951);
#6953=FILL_AREA_STYLE('',(#6952));
#6954=SURFACE_STYLE_FILL_AREA(#6953);
#6955=SURFACE_SIDE_STYLE('',(#6954));
#6956=SURFACE_STYLE_USAGE(.BOTH.,#6955);
#6957=PRESENTATION_STYLE_ASSIGNMENT((#6956));
ENDSEC;
END-ISO-10303-21;
